ISO-10303-21;
HEADER;
FILE_DESCRIPTION (('STEP AP214'),
    '1' );
FILE_NAME ('circlip for shafts normal_din_Circlip DIN 471 - 20 x 1.2.step',
    '2026-10-08T08:02:49',
    ( '' ),
    ( '' ),
    'SwSTEP 2.0',
    'SolidWorks 2026',
    '' );
FILE_SCHEMA (( 'AUTOMOTIVE_DESIGN' ));
ENDSEC;

DATA;
#13=SHAPE_REPRESENTATION ( 'circlip for shafts normal_din_Circlip DIN 471 - 20 x 1.2', ( #14677 ), #21841 ) ;
#49=EDGE_CURVE ( 'NONE', #23782, #28115, #2220, .T. ) ;
#117=LINE ( 'NONE', #14570, #16748 ) ;
#141=EDGE_CURVE ( 'NONE', #1542, #34181, #7863, .T. ) ;
#211=ORIENTED_EDGE ( 'NONE', *, *, #8364, .F. ) ;
#594=CARTESIAN_POINT ( 'NONE',  ( 1.600000000000000089, -11.64055411052240352, -1.199999999999999956 ) ) ;
#780=ADVANCED_FACE ( 'NONE', ( #41804 ), #54611, .F. ) ;
#866=LINE ( 'NONE', #10586, #42418 ) ;
#886=FACE_OUTER_BOUND ( 'NONE', #43567, .T. ) ;
#1043=DIRECTION ( 'NONE',  ( 1.000000000000000000, 0.000000000000000000, 0.000000000000000000 ) ) ;
#1059=ADVANCED_FACE ( 'NONE', ( #44575 ), #1610, .T. ) ;
#1064=ORIENTED_EDGE ( 'NONE', *, *, #141, .F. ) ;
#1137=FACE_OUTER_BOUND ( 'NONE', #50337, .T. ) ;
#1150=ORIENTED_EDGE ( 'NONE', *, *, #24042, .T. ) ;
#1468=DIRECTION ( 'NONE',  ( 1.000000000000000000, 0.000000000000000000, 0.000000000000000000 ) ) ;
#1542=VERTEX_POINT ( 'NONE', #53049 ) ;
#1610=CYLINDRICAL_SURFACE ( 'NONE', #37094, 11.40403086437694569 ) ;
#1715=CARTESIAN_POINT ( 'NONE',  ( 4.214292481396495482, -11.25702090725073035, -1.199999999999999956 ) ) ;
#1782=ORIENTED_EDGE ( 'NONE', *, *, #33899, .T. ) ;
#1803=DIRECTION ( 'NONE',  ( -0.000000000000000000, -0.000000000000000000, -1.000000000000000000 ) ) ;
#1885=EDGE_LOOP ( 'NONE', ( #25728, #31435 ) ) ;
#1903=CARTESIAN_POINT ( 'NONE',  ( 0.2111111111111110827, -9.497654031326126400, 0.000000000000000000 ) ) ;
#2109=CARTESIAN_POINT ( 'NONE',  ( -4.214292481396491930, -11.25702090725073035, -1.199999999999999956 ) ) ;
#2124=LINE ( 'NONE', #39775, #58597 ) ;
#2220=LINE ( 'NONE', #7539, #50037 ) ;
#2225=EDGE_LOOP ( 'NONE', ( #39572, #53306, #36706, #33179 ) ) ;
#2258=ORIENTED_EDGE ( 'NONE', *, *, #41131, .F. ) ;
#2322=ORIENTED_EDGE ( 'NONE', *, *, #27876, .F. ) ;
#2404=EDGE_LOOP ( 'NONE', ( #1064, #11527, #13683, #18976 ) ) ;
#2529=DIRECTION ( 'NONE',  ( 1.000000000000000000, 0.000000000000000000, 0.000000000000000000 ) ) ;
#2539=ORIENTED_EDGE ( 'NONE', *, *, #5894, .F. ) ;
#2606=CYLINDRICAL_SURFACE ( 'NONE', #2774, 1.000000000000000888 ) ;
#2639=EDGE_CURVE ( 'NONE', #50100, #8159, #22332, .T. ) ;
#2697=VECTOR ( 'NONE', #4936, 1000.000000000000000 ) ;
#2716=DIRECTION ( 'NONE',  ( 0.000000000000000000, 0.000000000000000000, 1.000000000000000000 ) ) ;
#2774=AXIS2_PLACEMENT_3D ( 'NONE', #40253, #59307, #16414 ) ;
#2836=VECTOR ( 'NONE', #3766, 1000.000000000000000 ) ;
#2842=ADVANCED_FACE ( 'NONE', ( #45174 ), #45784, .F. ) ;
#2855=VERTEX_POINT ( 'NONE', #1903 ) ;
#3206=LINE ( 'NONE', #17330, #12493 ) ;
#3279=CARTESIAN_POINT ( 'NONE',  ( 4.062725214796417461, -12.40828859588279798, -1.199999999999999956 ) ) ;
#3493=EDGE_LOOP ( 'NONE', ( #60611, #18515, #45500, #1782 ) ) ;
#3605=CARTESIAN_POINT ( 'NONE',  ( 0.2111111111111110827, -9.497654031326126400, -1.199999999999999956 ) ) ;
#3648=LINE ( 'NONE', #50654, #30953 ) ;
#3759=CARTESIAN_POINT ( 'NONE',  ( 0.000000000000000000, 0.000000000000000000, 0.000000000000000000 ) ) ;
#3766=DIRECTION ( 'NONE',  ( 0.000000000000000000, 0.000000000000000000, 1.000000000000000000 ) ) ;
#4307=DIRECTION ( 'NONE',  ( 1.000000000000000000, 0.000000000000000000, 0.000000000000000000 ) ) ;
#4405=FACE_OUTER_BOUND ( 'NONE', #21105, .T. ) ;
#4468=ORIENTED_EDGE ( 'NONE', *, *, #24042, .F. ) ;
#4495=DIRECTION ( 'NONE',  ( 1.000000000000000000, 0.000000000000000000, 0.000000000000000000 ) ) ;
#4573=AXIS2_PLACEMENT_3D ( 'NONE', #30505, #45268, #54303 ) ;
#4590=DIRECTION ( 'NONE',  ( 0.1305261922200468827, -0.9914448613738110483, 0.000000000000000000 ) ) ;
#4756=CARTESIAN_POINT ( 'NONE',  ( 0.5999999999999994227, -11.64055411052240352, -1.199999999999999956 ) ) ;
#4807=CIRCLE ( 'NONE', #8856, 13.50000000000000178 ) ;
#4845=DIRECTION ( 'NONE',  ( 1.000000000000000000, 0.000000000000000000, 0.000000000000000000 ) ) ;
#4847=ADVANCED_FACE ( 'NONE', ( #16657, #6283, #35463 ), #6913, .F. ) ;
#4852=CIRCLE ( 'NONE', #61910, 11.40403086437694569 ) ;
#4865=CARTESIAN_POINT ( 'NONE',  ( 1.600000000000000089, -11.64055411052240352, -1.199999999999999956 ) ) ;
#4936=DIRECTION ( 'NONE',  ( 0.000000000000000000, 0.000000000000000000, 1.000000000000000000 ) ) ;
#4973=LINE ( 'NONE', #61370, #48861 ) ;
#5153=CIRCLE ( 'NONE', #25162, 2.698940690764985550 ) ;
#5215=DIRECTION ( 'NONE',  ( 0.000000000000000000, 0.000000000000000000, 1.000000000000000000 ) ) ;
#5245=ORIENTED_EDGE ( 'NONE', *, *, #48085, .F. ) ;
#5388=CYLINDRICAL_SURFACE ( 'NONE', #6662, 11.40403086437694569 ) ;
#5459=CARTESIAN_POINT ( 'NONE',  ( 0.000000000000000000, 0.000000000000000000, 0.000000000000000000 ) ) ;
#5625=CARTESIAN_POINT ( 'NONE',  ( 0.000000000000000000, 0.6959691356230525150, -1.199999999999999956 ) ) ;
#5638=CIRCLE ( 'NONE', #29669, 2.698940690764988215 ) ;
#5657=VECTOR ( 'NONE', #34746, 1000.000000000000114 ) ;
#5698=VERTEX_POINT ( 'NONE', #59556 ) ;
#5787=VECTOR ( 'NONE', #10845, 1000.000000000000114 ) ;
#5818=ORIENTED_EDGE ( 'NONE', *, *, #8838, .T. ) ;
#5894=EDGE_CURVE ( 'NONE', #6658, #45408, #26985, .T. ) ;
#5895=PRESENTATION_STYLE_ASSIGNMENT (( #14727 ) ) ;
#5976=PRODUCT_DEFINITION_CONTEXT ( 'detailed design', #10377, 'design' ) ;
#6056=VERTEX_POINT ( 'NONE', #59170 ) ;
#6088=VERTEX_POINT ( 'NONE', #34778 ) ;
#6175=AXIS2_PLACEMENT_3D ( 'NONE', #12324, #26708, #31730 ) ;
#6203=SURFACE_STYLE_FILL_AREA ( #19735 ) ;
#6280=VERTEX_POINT ( 'NONE', #53169 ) ;
#6283=FACE_BOUND ( 'NONE', #18002, .T. ) ;
#6350=VERTEX_POINT ( 'NONE', #16511 ) ;
#6549=DIRECTION ( 'NONE',  ( 0.000000000000000000, 0.000000000000000000, 1.000000000000000000 ) ) ;
#6658=VERTEX_POINT ( 'NONE', #14602 ) ;
#6662=AXIS2_PLACEMENT_3D ( 'NONE', #56785, #9183, #10115 ) ;
#6700=CARTESIAN_POINT ( 'NONE',  ( 9.500000000000000000, 0.000000000000000000, -1.199999999999999956 ) ) ;
#6701=AXIS2_PLACEMENT_3D ( 'NONE', #8405, #32866, #4307 ) ;
#6782=ORIENTED_EDGE ( 'NONE', *, *, #30805, .F. ) ;
#6848=CARTESIAN_POINT ( 'NONE',  ( 9.500000000000000000, 0.000000000000000000, -1.199999999999999956 ) ) ;
#6913=PLANE ( 'NONE',  #53928 ) ;
#7071=ADVANCED_FACE ( 'NONE', ( #55998 ), #61006, .T. ) ;
#7097=DIRECTION ( 'NONE',  ( 0.1305261922200468827, -0.9914448613738110483, 0.000000000000000000 ) ) ;
#7210=DIRECTION ( 'NONE',  ( 0.000000000000000000, 0.000000000000000000, 1.000000000000000000 ) ) ;
#7222=DIRECTION ( 'NONE',  ( 0.000000000000000000, 0.000000000000000000, 1.000000000000000000 ) ) ;
#7243=DIRECTION ( 'NONE',  ( 0.000000000000000000, 0.000000000000000000, 1.000000000000000000 ) ) ;
#7268=DIRECTION ( 'NONE',  ( 0.000000000000000000, 0.000000000000000000, 1.000000000000000000 ) ) ;
#7379=ORIENTED_EDGE ( 'NONE', *, *, #8627, .T. ) ;
#7385=VERTEX_POINT ( 'NONE', #6848 ) ;
#7539=CARTESIAN_POINT ( 'NONE',  ( -11.40403086437694569, 0.6959691356230539583, -1.199999999999999956 ) ) ;
#7863=LINE ( 'NONE', #59553, #38085 ) ;
#7964=ORIENTED_EDGE ( 'NONE', *, *, #36102, .F. ) ;
#8004=ORIENTED_EDGE ( 'NONE', *, *, #2639, .F. ) ;
#8159=VERTEX_POINT ( 'NONE', #57390 ) ;
#8364=EDGE_CURVE ( 'NONE', #22852, #26491, #50790, .T. ) ;
#8405=CARTESIAN_POINT ( 'NONE',  ( 0.000000000000000000, 0.6959691356230525150, 0.000000000000000000 ) ) ;
#8510=FACE_OUTER_BOUND ( 'NONE', #2404, .T. ) ;
#8627=EDGE_CURVE ( 'NONE', #50100, #6088, #60470, .T. ) ;
#8669=EDGE_CURVE ( 'NONE', #22852, #50100, #22234, .T. ) ;
#8699=CARTESIAN_POINT ( 'NONE',  ( -0.5999999999999992006, -11.64055411052240352, 0.000000000000000000 ) ) ;
#8795=ORIENTED_EDGE ( 'NONE', *, *, #50444, .T. ) ;
#8820=EDGE_LOOP ( 'NONE', ( #35334, #23438, #54149, #26586, #53475, #36247, #53939, #33039, #39499, #36197, #28900, #16415, #54154, #61632, #47114, #21323 ) ) ;
#8838=EDGE_CURVE ( 'NONE', #6280, #38091, #55467, .T. ) ;
#8856=AXIS2_PLACEMENT_3D ( 'NONE', #61433, #23252, #33586 ) ;
#9114=EDGE_CURVE ( 'NONE', #28847, #31387, #58453, .T. ) ;
#9183=DIRECTION ( 'NONE',  ( 0.000000000000000000, 0.000000000000000000, 1.000000000000000000 ) ) ;
#9212=CARTESIAN_POINT ( 'NONE',  ( -1.600000000000000089, -11.64055411052240352, 0.000000000000000000 ) ) ;
#9230=DIRECTION ( 'NONE',  ( 0.000000000000000000, 0.000000000000000000, 1.000000000000000000 ) ) ;
#9459=AXIS2_PLACEMENT_3D ( 'NONE', #4865, #54949, #35261 ) ;
#9512=ORIENTED_EDGE ( 'NONE', *, *, #54654, .T. ) ;
#9714=ORIENTED_EDGE ( 'NONE', *, *, #38801, .T. ) ;
#9723=DIRECTION ( 'NONE',  ( 1.000000000000000000, 0.000000000000000000, 0.000000000000000000 ) ) ;
#9739=CARTESIAN_POINT ( 'NONE',  ( 5.571549742892842438, -9.254395351074542475, -1.199999999999999956 ) ) ;
#9764=ADVANCED_FACE ( 'NONE', ( #886 ), #20928, .T. ) ;
#9885=CARTESIAN_POINT ( 'NONE',  ( 0.000000000000000000, 0.000000000000000000, -1.199999999999999956 ) ) ;
#9964=DIRECTION ( 'NONE',  ( 0.9997530559290660479, -0.02222222222222222307, 0.000000000000000000 ) ) ;
#9970=ORIENTED_EDGE ( 'NONE', *, *, #49268, .F. ) ;
#10091=DIRECTION ( 'NONE',  ( 1.000000000000000000, 0.000000000000000000, 0.000000000000000000 ) ) ;
#10115=DIRECTION ( 'NONE',  ( 1.000000000000000000, 0.000000000000000000, 0.000000000000000000 ) ) ;
#10307=DIRECTION ( 'NONE',  ( 0.1305261922200468827, -0.9914448613738110483, 0.000000000000000000 ) ) ;
#10324=DIRECTION ( 'NONE',  ( 1.000000000000000000, 0.000000000000000000, 0.000000000000000000 ) ) ;
#10345=DIRECTION ( 'NONE',  ( -0.000000000000000000, -0.000000000000000000, -1.000000000000000000 ) ) ;
#10377=APPLICATION_CONTEXT ( 'automotive_design' ) ;
#10421=ORIENTED_EDGE ( 'NONE', *, *, #36102, .T. ) ;
#10566=VERTEX_POINT ( 'NONE', #45464 ) ;
#10586=CARTESIAN_POINT ( 'NONE',  ( 5.571549742892842438, -9.254395351074542475, -1.199999999999999956 ) ) ;
#10626=( NAMED_UNIT ( * ) SI_UNIT ( $, .STERADIAN. ) SOLID_ANGLE_UNIT ( ) );
#10661=ORIENTED_EDGE ( 'NONE', *, *, #44884, .T. ) ;
#10794=ORIENTED_EDGE ( 'NONE', *, *, #50904, .F. ) ;
#10808=DIRECTION ( 'NONE',  ( 1.000000000000000000, 0.000000000000000000, 0.000000000000000000 ) ) ;
#10845=DIRECTION ( 'NONE',  ( 0.1305261922200498526, 0.9914448613738106042, -0.000000000000000000 ) ) ;
#10894=PRODUCT_DEFINITION_FORMATION_WITH_SPECIFIED_SOURCE ( 'ANY', '', #54756, .NOT_KNOWN. ) ;
#10984=CARTESIAN_POINT ( 'NONE',  ( 0.5999999999999994227, -11.64055411052240352, -1.199999999999999956 ) ) ;
#10994=DIRECTION ( 'NONE',  ( 0.000000000000000000, 0.000000000000000000, 1.000000000000000000 ) ) ;
#11002=VERTEX_POINT ( 'NONE', #47532 ) ;
#11060=CIRCLE ( 'NONE', #34058, 11.40403086437694569 ) ;
#11143=DIRECTION ( 'NONE',  ( 0.000000000000000000, 0.000000000000000000, 1.000000000000000000 ) ) ;
#11348=EDGE_CURVE ( 'NONE', #6280, #5698, #117, .T. ) ;
#11394=CARTESIAN_POINT ( 'NONE',  ( 0.2999999999999897193, -13.49666625504239192, 0.000000000000000000 ) ) ;
#11523=DIRECTION ( 'NONE',  ( 0.000000000000000000, 0.000000000000000000, 1.000000000000000000 ) ) ;
#11527=ORIENTED_EDGE ( 'NONE', *, *, #34175, .F. ) ;
#11595=AXIS2_PLACEMENT_3D ( 'NONE', #29397, #1803, #57570 ) ;
#11612=ORIENTED_EDGE ( 'NONE', *, *, #34820, .F. ) ;
#11615=ORIENTED_EDGE ( 'NONE', *, *, #15386, .T. ) ;
#11835=CIRCLE ( 'NONE', #45867, 1.000000000000000888 ) ;
#12010=DIRECTION ( 'NONE',  ( 0.000000000000000000, 0.000000000000000000, 1.000000000000000000 ) ) ;
#12139=FACE_OUTER_BOUND ( 'NONE', #48808, .T. ) ;
#12324=CARTESIAN_POINT ( 'NONE',  ( 3.319141568766058814, -12.31039395171775830, -1.199999999999999956 ) ) ;
#12389=CARTESIAN_POINT ( 'NONE',  ( -0.2999999999999999889, -13.49666625504239015, 0.000000000000000000 ) ) ;
#12485=ADVANCED_FACE ( 'NONE', ( #31751 ), #2606, .F. ) ;
#12493=VECTOR ( 'NONE', #21098, 1000.000000000000000 ) ;
#12632=CARTESIAN_POINT ( 'NONE',  ( -5.571549742892843327, -9.254395351074540699, -1.199999999999999956 ) ) ;
#12682=ORIENTED_EDGE ( 'NONE', *, *, #54946, .F. ) ;
#12850=CARTESIAN_POINT ( 'NONE',  ( 0.000000000000000000, 0.000000000000000000, -1.199999999999999956 ) ) ;
#12886=DIRECTION ( 'NONE',  ( -0.000000000000000000, -0.000000000000000000, -1.000000000000000000 ) ) ;
#12941=LINE ( 'NONE', #12632, #49822 ) ;
#12950=VECTOR ( 'NONE', #56350, 1000.000000000000000 ) ;
#13051=ORIENTED_EDGE ( 'NONE', *, *, #11348, .F. ) ;
#13325=FACE_OUTER_BOUND ( 'NONE', #38813, .T. ) ;
#13347=VECTOR ( 'NONE', #47381, 1000.000000000000000 ) ;
#13348=DIRECTION ( 'NONE',  ( 1.000000000000000000, 0.000000000000000000, 0.000000000000000000 ) ) ;
#13353=DIRECTION ( 'NONE',  ( 0.02222222222222222307, -0.9997530559290660479, 0.000000000000000000 ) ) ;
#13683=ORIENTED_EDGE ( 'NONE', *, *, #26361, .T. ) ;
#13696=VERTEX_POINT ( 'NONE', #23181 ) ;
#13822=DIRECTION ( 'NONE',  ( 1.000000000000000000, 0.000000000000000000, 0.000000000000000000 ) ) ;
#13855=EDGE_CURVE ( 'NONE', #26491, #8159, #2124, .T. ) ;
#13907=LINE ( 'NONE', #4756, #43764 ) ;
#14008=AXIS2_PLACEMENT_3D ( 'NONE', #33470, #9964, #58162 ) ;
#14040=DIRECTION ( 'NONE',  ( 0.000000000000000000, 0.000000000000000000, 1.000000000000000000 ) ) ;
#14147=VECTOR ( 'NONE', #46778, 1000.000000000000000 ) ;
#14186=CIRCLE ( 'NONE', #49176, 0.7500000000000015543 ) ;
#14300=ORIENTED_EDGE ( 'NONE', *, *, #56980, .F. ) ;
#14363=PLANE ( 'NONE',  #14008 ) ;
#14570=CARTESIAN_POINT ( 'NONE',  ( 2.600000000000000533, -11.64055411052240352, -1.199999999999999956 ) ) ;
#14593=AXIS2_PLACEMENT_3D ( 'NONE', #5459, #52780, #57154 ) ;
#14602=CARTESIAN_POINT ( 'NONE',  ( -4.062725214796418349, -12.40828859588279798, -1.199999999999999956 ) ) ;
#14677=AXIS2_PLACEMENT_3D ( 'NONE', #3759, #61387, #13822 ) ;
#14727=SURFACE_STYLE_USAGE ( .BOTH. , #25348 ) ;
#14823=EDGE_CURVE ( 'NONE', #28115, #24133, #31667, .T. ) ;
#14866=CYLINDRICAL_SURFACE ( 'NONE', #25740, 1.000000000000000888 ) ;
#14951=CIRCLE ( 'NONE', #51986, 9.500000000000000000 ) ;
#15012=DIRECTION ( 'NONE',  ( 1.000000000000000000, 0.000000000000000000, 0.000000000000000000 ) ) ;
#15167=CARTESIAN_POINT ( 'NONE',  ( -11.40403086437694569, 0.6959691356230539583, -1.199999999999999956 ) ) ;
#15285=FACE_OUTER_BOUND ( 'NONE', #39314, .T. ) ;
#15297=AXIS2_PLACEMENT_3D ( 'NONE', #49525, #44864, #10091 ) ;
#15313=ORIENTED_EDGE ( 'NONE', *, *, #26763, .T. ) ;
#15381=ADVANCED_FACE ( 'NONE', ( #26815, #27424, #60304 ), #36232, .T. ) ;
#15386=EDGE_CURVE ( 'NONE', #6658, #39805, #35202, .T. ) ;
#15642=( NAMED_UNIT ( * ) PLANE_ANGLE_UNIT ( ) SI_UNIT ( $, .RADIAN. ) );
#15646=EDGE_CURVE ( 'NONE', #34181, #38682, #5153, .T. ) ;
#15700=CARTESIAN_POINT ( 'NONE',  ( 0.000000000000000000, 0.000000000000000000, -1.199999999999999956 ) ) ;
#15815=DIRECTION ( 'NONE',  ( 0.000000000000000000, 0.000000000000000000, 1.000000000000000000 ) ) ;
#15925=DIRECTION ( 'NONE',  ( 1.000000000000000000, 0.000000000000000000, 0.000000000000000000 ) ) ;
#16053=CARTESIAN_POINT ( 'NONE',  ( 0.000000000000000000, 0.6959691356230525150, -1.199999999999999956 ) ) ;
#16116=CARTESIAN_POINT ( 'NONE',  ( 6.890143360408123030, -11.60930335864404306, 0.000000000000000000 ) ) ;
#16269=( GEOMETRIC_REPRESENTATION_CONTEXT ( 3 ) GLOBAL_UNCERTAINTY_ASSIGNED_CONTEXT ( ( #36784 ) ) GLOBAL_UNIT_ASSIGNED_CONTEXT ( ( #43873, #53828, #44795 ) ) REPRESENTATION_CONTEXT ( 'NONE', 'WORKASPACE' ) );
#16414=DIRECTION ( 'NONE',  ( 1.000000000000000000, 0.000000000000000000, 0.000000000000000000 ) ) ;
#16415=ORIENTED_EDGE ( 'NONE', *, *, #37814, .T. ) ;
#16439=ADVANCED_FACE ( 'NONE', ( #45531 ), #59596, .T. ) ;
#16447=LINE ( 'NONE', #6700, #47546 ) ;
#16511=CARTESIAN_POINT ( 'NONE',  ( 0.2111111111111110827, -9.497654031326126400, -1.199999999999999956 ) ) ;
#16657=FACE_BOUND ( 'NONE', #53248, .T. ) ;
#16748=VECTOR ( 'NONE', #9230, 1000.000000000000000 ) ;
#16851=CARTESIAN_POINT ( 'NONE',  ( 4.214292481396495482, -11.25702090725073035, -1.199999999999999956 ) ) ;
#17079=ORIENTED_EDGE ( 'NONE', *, *, #59875, .T. ) ;
#17190=CARTESIAN_POINT ( 'NONE',  ( 11.40403086437694569, 0.6959691356230525150, -1.199999999999999956 ) ) ;
#17330=CARTESIAN_POINT ( 'NONE',  ( 11.40403086437694569, 0.6959691356230525150, -1.199999999999999956 ) ) ;
#17624=EDGE_CURVE ( 'NONE', #11002, #45408, #22461, .T. ) ;
#17761=CARTESIAN_POINT ( 'NONE',  ( 0.000000000000000000, 0.000000000000000000, -1.199999999999999956 ) ) ;
#17951=VECTOR ( 'NONE', #19397, 1000.000000000000000 ) ;
#18002=EDGE_LOOP ( 'NONE', ( #5818, #35788 ) ) ;
#18088=DIRECTION ( 'NONE',  ( 0.000000000000000000, 0.000000000000000000, 1.000000000000000000 ) ) ;
#18091=ORIENTED_EDGE ( 'NONE', *, *, #61036, .F. ) ;
#18113=DIRECTION ( 'NONE',  ( -0.9914448613738110483, -0.1305261922200468827, 0.000000000000000000 ) ) ;
#18242=ORIENTED_EDGE ( 'NONE', *, *, #8364, .T. ) ;
#18359=DIRECTION ( 'NONE',  ( 1.000000000000000000, 0.000000000000000000, -0.000000000000000000 ) ) ;
#18515=ORIENTED_EDGE ( 'NONE', *, *, #26763, .F. ) ;
#18976=ORIENTED_EDGE ( 'NONE', *, *, #39855, .T. ) ;
#19244=VERTEX_POINT ( 'NONE', #51664 ) ;
#19261=CARTESIAN_POINT ( 'NONE',  ( 0.000000000000000000, 0.000000000000000000, 0.000000000000000000 ) ) ;
#19283=MECHANICAL_DESIGN_GEOMETRIC_PRESENTATION_REPRESENTATION('',(#61275),#16269);
#19397=DIRECTION ( 'NONE',  ( 0.000000000000000000, 0.000000000000000000, 1.000000000000000000 ) ) ;
#19408=CARTESIAN_POINT ( 'NONE',  ( -5.571549742892843327, -9.254395351074540699, 0.000000000000000000 ) ) ;
#19536=DIRECTION ( 'NONE',  ( 0.000000000000000000, 0.000000000000000000, 1.000000000000000000 ) ) ;
#19679=VECTOR ( 'NONE', #11523, 1000.000000000000000 ) ;
#19735=FILL_AREA_STYLE ('',( #34761 ) ) ;
#19784=DIRECTION ( 'NONE',  ( 0.000000000000000000, 0.000000000000000000, 1.000000000000000000 ) ) ;
#19928=ORIENTED_EDGE ( 'NONE', *, *, #36445, .F. ) ;
#19966=EDGE_CURVE ( 'NONE', #6350, #36253, #25032, .T. ) ;
#20050=AXIS2_PLACEMENT_3D ( 'NONE', #44408, #5215, #23186 ) ;
#20128=AXIS2_PLACEMENT_3D ( 'NONE', #20411, #7210, #20720 ) ;
#20204=EDGE_LOOP ( 'NONE', ( #45252, #10661, #41242, #22769 ) ) ;
#20384=DIRECTION ( 'NONE',  ( 1.000000000000000000, 0.000000000000000000, 0.000000000000000000 ) ) ;
#20411=CARTESIAN_POINT ( 'NONE',  ( 0.000000000000000000, 0.000000000000000000, -1.199999999999999956 ) ) ;
#20720=DIRECTION ( 'NONE',  ( 1.000000000000000000, 0.000000000000000000, 0.000000000000000000 ) ) ;
#20740=CIRCLE ( 'NONE', #6701, 11.40403086437694569 ) ;
#20928=CYLINDRICAL_SURFACE ( 'NONE', #52523, 13.50000000000000178 ) ;
#20981=VERTEX_POINT ( 'NONE', #17190 ) ;
#21098=DIRECTION ( 'NONE',  ( 0.000000000000000000, 0.000000000000000000, 1.000000000000000000 ) ) ;
#21105=EDGE_LOOP ( 'NONE', ( #22671, #53600, #24315, #52394 ) ) ;
#21278=ADVANCED_BREP_SHAPE_REPRESENTATION ( '', ( #31244, #14677 ), #21841 ) ;
#21323=ORIENTED_EDGE ( 'NONE', *, *, #13855, .T. ) ;
#21512=CYLINDRICAL_SURFACE ( 'NONE', #39014, 13.50000000000000178 ) ;
#21745=CARTESIAN_POINT ( 'NONE',  ( 9.500000000000000000, 0.000000000000000000, 0.000000000000000000 ) ) ;
#21841=( GEOMETRIC_REPRESENTATION_CONTEXT ( 3 ) GLOBAL_UNCERTAINTY_ASSIGNED_CONTEXT ( ( #23577 ) ) GLOBAL_UNIT_ASSIGNED_CONTEXT ( ( #58512, #30330, #10626 ) ) REPRESENTATION_CONTEXT ( 'NONE', 'WORKASPACE' ) );
#21847=DIRECTION ( 'NONE',  ( 1.000000000000000000, 0.000000000000000000, 0.000000000000000000 ) ) ;
#22046=ORIENTED_EDGE ( 'NONE', *, *, #19966, .T. ) ;
#22078=DIRECTION ( 'NONE',  ( 1.000000000000000000, 0.000000000000000000, 0.000000000000000000 ) ) ;
#22234=LINE ( 'NONE', #36044, #41508 ) ;
#22332=LINE ( 'NONE', #56751, #14147 ) ;
#22427=PLANE ( 'NONE',  #38333 ) ;
#22461=LINE ( 'NONE', #41585, #29227 ) ;
#22548=AXIS2_PLACEMENT_3D ( 'NONE', #17761, #2716, #37193 ) ;
#22589=CIRCLE ( 'NONE', #11595, 9.500000000000000000 ) ;
#22671=ORIENTED_EDGE ( 'NONE', *, *, #15646, .F. ) ;
#22769=ORIENTED_EDGE ( 'NONE', *, *, #59754, .F. ) ;
#22852=VERTEX_POINT ( 'NONE', #61769 ) ;
#22863=ADVANCED_FACE ( 'NONE', ( #52647 ), #29162, .F. ) ;
#22967=ORIENTED_EDGE ( 'NONE', *, *, #38713, .F. ) ;
#23015=FACE_OUTER_BOUND ( 'NONE', #3493, .T. ) ;
#23033=CYLINDRICAL_SURFACE ( 'NONE', #54897, 0.7500000000000015543 ) ;
#23113=EDGE_CURVE ( 'NONE', #55532, #28847, #61658, .T. ) ;
#23181=CARTESIAN_POINT ( 'NONE',  ( -4.214292481396491930, -11.25702090725073035, -1.199999999999999956 ) ) ;
#23186=DIRECTION ( 'NONE',  ( 1.000000000000000000, 0.000000000000000000, 0.000000000000000000 ) ) ;
#23213=DIRECTION ( 'NONE',  ( 0.000000000000000000, 0.000000000000000000, 1.000000000000000000 ) ) ;
#23252=DIRECTION ( 'NONE',  ( 0.000000000000000000, 0.000000000000000000, 1.000000000000000000 ) ) ;
#23265=CARTESIAN_POINT ( 'NONE',  ( 0.2111111111111110827, -9.497654031326126400, 0.000000000000000000 ) ) ;
#23271=EDGE_CURVE ( 'NONE', #6350, #2855, #24707, .T. ) ;
#23434=AXIS2_PLACEMENT_3D ( 'NONE', #55334, #31547, #21847 ) ;
#23438=ORIENTED_EDGE ( 'NONE', *, *, #59754, .T. ) ;
#23460=EDGE_CURVE ( 'NONE', #36253, #56952, #3648, .T. ) ;
#23474=DIRECTION ( 'NONE',  ( 0.000000000000000000, 0.000000000000000000, 1.000000000000000000 ) ) ;
#23477=VERTEX_POINT ( 'NONE', #60660 ) ;
#23534=APPLICATION_CONTEXT ( 'automotive_design' ) ;
#23577=UNCERTAINTY_MEASURE_WITH_UNIT (LENGTH_MEASURE( 1.000000000000000082E-05 ), #58512, 'distance_accuracy_value', 'NONE');
#23593=FACE_OUTER_BOUND ( 'NONE', #54792, .T. ) ;
#23623=DIRECTION ( 'NONE',  ( 0.000000000000000000, 0.000000000000000000, 1.000000000000000000 ) ) ;
#23701=EDGE_LOOP ( 'NONE', ( #12682, #48932, #26531, #36226 ) ) ;
#23770=EDGE_LOOP ( 'NONE', ( #18091, #28523, #30716, #9970 ) ) ;
#23782=VERTEX_POINT ( 'NONE', #15167 ) ;
#23901=DIRECTION ( 'NONE',  ( 0.000000000000000000, 0.000000000000000000, 1.000000000000000000 ) ) ;
#23979=CYLINDRICAL_SURFACE ( 'NONE', #27979, 9.500000000000000000 ) ;
#24042=EDGE_CURVE ( 'NONE', #45559, #55532, #52978, .T. ) ;
#24133=VERTEX_POINT ( 'NONE', #19408 ) ;
#24315=ORIENTED_EDGE ( 'NONE', *, *, #42871, .T. ) ;
#24509=DIRECTION ( 'NONE',  ( 0.000000000000000000, 0.000000000000000000, 1.000000000000000000 ) ) ;
#24707=LINE ( 'NONE', #53796, #17951 ) ;
#24728=DIRECTION ( 'NONE',  ( 0.000000000000000000, 0.000000000000000000, 1.000000000000000000 ) ) ;
#25032=LINE ( 'NONE', #58514, #5657 ) ;
#25162=AXIS2_PLACEMENT_3D ( 'NONE', #16116, #60460, #34925 ) ;
#25267=CYLINDRICAL_SURFACE ( 'NONE', #20050, 11.40403086437694569 ) ;
#25295=CARTESIAN_POINT ( 'NONE',  ( -3.319141568766058814, -12.31039395171775830, 0.000000000000000000 ) ) ;
#25310=ADVANCED_FACE ( 'NONE', ( #1137 ), #25267, .T. ) ;
#25348=SURFACE_SIDE_STYLE ('',( #6203 ) ) ;
#25417=CARTESIAN_POINT ( 'NONE',  ( 0.000000000000000000, 0.000000000000000000, -1.199999999999999956 ) ) ;
#25423=EDGE_CURVE ( 'NONE', #55303, #28115, #11060, .T. ) ;
#25706=AXIS2_PLACEMENT_3D ( 'NONE', #37126, #51485, #22078 ) ;
#25728=ORIENTED_EDGE ( 'NONE', *, *, #26667, .F. ) ;
#25740=AXIS2_PLACEMENT_3D ( 'NONE', #34898, #34276, #1043 ) ;
#25954=PRESENTATION_STYLE_ASSIGNMENT (( #45391 ) ) ;
#26005=PRODUCT_DEFINITION ( 'UNKNOWN', '', #10894, #5976 ) ;
#26020=AXIS2_PLACEMENT_3D ( 'NONE', #25295, #44442, #1468 ) ;
#26130=DIRECTION ( 'NONE',  ( 0.000000000000000000, 0.000000000000000000, 1.000000000000000000 ) ) ;
#26183=DIRECTION ( 'NONE',  ( 0.000000000000000000, 0.000000000000000000, 1.000000000000000000 ) ) ;
#26194=FACE_OUTER_BOUND ( 'NONE', #26278, .T. ) ;
#26278=EDGE_LOOP ( 'NONE', ( #29168, #39820, #22046, #41055 ) ) ;
#26336=LINE ( 'NONE', #31352, #47437 ) ;
#26361=EDGE_CURVE ( 'NONE', #53602, #57538, #49969, .T. ) ;
#26396=DIRECTION ( 'NONE',  ( -1.000000000000000000, 0.000000000000000000, 0.000000000000000000 ) ) ;
#26491=VERTEX_POINT ( 'NONE', #12389 ) ;
#26493=DIRECTION ( 'NONE',  ( 1.000000000000000000, 0.000000000000000000, 0.000000000000000000 ) ) ;
#26531=ORIENTED_EDGE ( 'NONE', *, *, #23271, .T. ) ;
#26586=ORIENTED_EDGE ( 'NONE', *, *, #34671, .T. ) ;
#26667=EDGE_CURVE ( 'NONE', #31387, #28847, #11835, .T. ) ;
#26708=DIRECTION ( 'NONE',  ( 0.000000000000000000, 0.000000000000000000, 1.000000000000000000 ) ) ;
#26763=EDGE_CURVE ( 'NONE', #23477, #24133, #12941, .T. ) ;
#26815=FACE_BOUND ( 'NONE', #1885, .T. ) ;
#26957=ADVANCED_FACE ( 'NONE', ( #4405 ), #27633, .F. ) ;
#26985=LINE ( 'NONE', #41416, #2836 ) ;
#27326=CARTESIAN_POINT ( 'NONE',  ( 3.319141568766058814, -12.31039395171775830, 0.000000000000000000 ) ) ;
#27424=FACE_BOUND ( 'NONE', #31785, .T. ) ;
#27493=AXIS2_PLACEMENT_3D ( 'NONE', #38314, #57365, #52682 ) ;
#27633=CYLINDRICAL_SURFACE ( 'NONE', #52807, 2.698940690764985550 ) ;
#27636=DIRECTION ( 'NONE',  ( 0.1305261922200498248, 0.9914448613738106042, 0.000000000000000000 ) ) ;
#27876=EDGE_CURVE ( 'NONE', #36253, #19244, #4807, .T. ) ;
#27979=AXIS2_PLACEMENT_3D ( 'NONE', #9885, #33091, #4845 ) ;
#28115=VERTEX_POINT ( 'NONE', #45168 ) ;
#28146=ORIENTED_EDGE ( 'NONE', *, *, #58060, .F. ) ;
#28288=DIRECTION ( 'NONE',  ( 1.000000000000000000, 0.000000000000000000, 0.000000000000000000 ) ) ;
#28416=VECTOR ( 'NONE', #38160, 1000.000000000000000 ) ;
#28419=CARTESIAN_POINT ( 'NONE',  ( -4.214292481396491930, -11.25702090725073035, -1.199999999999999956 ) ) ;
#28519=ORIENTED_EDGE ( 'NONE', *, *, #8669, .T. ) ;
#28523=ORIENTED_EDGE ( 'NONE', *, *, #23113, .T. ) ;
#28557=CIRCLE ( 'NONE', #32564, 13.50000000000000178 ) ;
#28650=CARTESIAN_POINT ( 'NONE',  ( -0.2111111111111110827, -9.497654031326126400, -1.199999999999999956 ) ) ;
#28666=AXIS2_PLACEMENT_3D ( 'NONE', #33839, #24728, #10324 ) ;
#28712=VERTEX_POINT ( 'NONE', #9739 ) ;
#28804=EDGE_CURVE ( 'NONE', #23782, #23477, #4852, .T. ) ;
#28847=VERTEX_POINT ( 'NONE', #30378 ) ;
#28880=LINE ( 'NONE', #23265, #36187 ) ;
#28900=ORIENTED_EDGE ( 'NONE', *, *, #14823, .T. ) ;
#29162=CYLINDRICAL_SURFACE ( 'NONE', #61951, 9.500000000000000000 ) ;
#29168=ORIENTED_EDGE ( 'NONE', *, *, #34671, .F. ) ;
#29227=VECTOR ( 'NONE', #7097, 1000.000000000000114 ) ;
#29341=CARTESIAN_POINT ( 'NONE',  ( -3.514385190458188646, -13.03453477240703862, -1.199999999999999956 ) ) ;
#29393=DIRECTION ( 'NONE',  ( 0.000000000000000000, 0.000000000000000000, 1.000000000000000000 ) ) ;
#29397=CARTESIAN_POINT ( 'NONE',  ( 0.000000000000000000, 0.000000000000000000, 0.000000000000000000 ) ) ;
#29476=EDGE_CURVE ( 'NONE', #60067, #2855, #56919, .T. ) ;
#29482=ADVANCED_FACE ( 'NONE', ( #13325 ), #23033, .T. ) ;
#29669=AXIS2_PLACEMENT_3D ( 'NONE', #33053, #52125, #4495 ) ;
#29678=DIRECTION ( 'NONE',  ( 0.000000000000000000, 0.000000000000000000, 1.000000000000000000 ) ) ;
#29830=( GEOMETRIC_REPRESENTATION_CONTEXT ( 3 ) GLOBAL_UNCERTAINTY_ASSIGNED_CONTEXT ( ( #61161 ) ) GLOBAL_UNIT_ASSIGNED_CONTEXT ( ( #39456, #15642, #30026 ) ) REPRESENTATION_CONTEXT ( 'NONE', 'WORKASPACE' ) );
#29897=AXIS2_PLACEMENT_3D ( 'NONE', #56654, #57879, #38506 ) ;
#30012=CARTESIAN_POINT ( 'NONE',  ( 0.000000000000000000, 0.000000000000000000, -1.199999999999999956 ) ) ;
#30026=( NAMED_UNIT ( * ) SI_UNIT ( $, .STERADIAN. ) SOLID_ANGLE_UNIT ( ) );
#30043=CYLINDRICAL_SURFACE ( 'NONE', #39318, 1.000000000000000666 ) ;
#30052=ORIENTED_EDGE ( 'NONE', *, *, #46158, .F. ) ;
#30330=( NAMED_UNIT ( * ) PLANE_ANGLE_UNIT ( ) SI_UNIT ( $, .RADIAN. ) );
#30378=CARTESIAN_POINT ( 'NONE',  ( -2.600000000000000533, -11.64055411052240352, 0.000000000000000000 ) ) ;
#30387=CARTESIAN_POINT ( 'NONE',  ( -2.600000000000000533, -11.64055411052240352, -1.199999999999999956 ) ) ;
#30420=DIRECTION ( 'NONE',  ( 1.000000000000000000, 0.000000000000000000, -0.000000000000000000 ) ) ;
#30428=EDGE_LOOP ( 'NONE', ( #7379, #8795, #37904, #8004 ) ) ;
#30505=CARTESIAN_POINT ( 'NONE',  ( 0.000000000000000000, 0.6959691356230525150, -1.199999999999999956 ) ) ;
#30589=DIRECTION ( 'NONE',  ( 1.000000000000000000, 0.000000000000000000, 0.000000000000000000 ) ) ;
#30716=ORIENTED_EDGE ( 'NONE', *, *, #9114, .T. ) ;
#30805=EDGE_CURVE ( 'NONE', #56952, #56336, #36275, .T. ) ;
#30822=CARTESIAN_POINT ( 'NONE',  ( 1.600000000000000089, -11.64055411052240352, -1.199999999999999956 ) ) ;
#30929=ORIENTED_EDGE ( 'NONE', *, *, #14823, .F. ) ;
#30953=VECTOR ( 'NONE', #18088, 1000.000000000000000 ) ;
#30961=SHAPE_REPRESENTATION_RELATIONSHIP ( 'NONE' , 'NONE' ,  #13, #21278 ) ;
#31008=DIRECTION ( 'NONE',  ( 0.02222222222222222307, 0.9997530559290660479, -0.000000000000000000 ) ) ;
#31079=ORIENTED_EDGE ( 'NONE', *, *, #49, .T. ) ;
#31153=AXIS2_PLACEMENT_3D ( 'NONE', #36857, #37470, #13348 ) ;
#31220=CARTESIAN_POINT ( 'NONE',  ( -4.062725214796418349, -12.40828859588279798, 0.000000000000000000 ) ) ;
#31242=ADVANCED_FACE ( 'NONE', ( #38542 ), #30043, .F. ) ;
#31244=MANIFOLD_SOLID_BREP ( 'Body', #61019 ) ;
#31300=ORIENTED_EDGE ( 'NONE', *, *, #49268, .T. ) ;
#31352=CARTESIAN_POINT ( 'NONE',  ( -4.214292481396491930, -11.25702090725073035, -1.199999999999999956 ) ) ;
#31387=VERTEX_POINT ( 'NONE', #8699 ) ;
#31412=DIRECTION ( 'NONE',  ( 0.000000000000000000, 0.000000000000000000, 1.000000000000000000 ) ) ;
#31435=ORIENTED_EDGE ( 'NONE', *, *, #9114, .F. ) ;
#31467=AXIS2_PLACEMENT_3D ( 'NONE', #59578, #12010, #35186 ) ;
#31547=DIRECTION ( 'NONE',  ( -0.000000000000000000, -0.000000000000000000, -1.000000000000000000 ) ) ;
#31667=CIRCLE ( 'NONE', #28666, 11.40403086437694569 ) ;
#31725=ADVANCED_FACE ( 'NONE', ( #26194 ), #22427, .T. ) ;
#31730=DIRECTION ( 'NONE',  ( 1.000000000000000000, 0.000000000000000000, 0.000000000000000000 ) ) ;
#31751=FACE_OUTER_BOUND ( 'NONE', #39648, .T. ) ;
#31785=EDGE_LOOP ( 'NONE', ( #47909, #28146 ) ) ;
#31823=LINE ( 'NONE', #3279, #60420 ) ;
#31880=ADVANCED_FACE ( 'NONE', ( #8510 ), #42078, .T. ) ;
#31927=ORIENTED_EDGE ( 'NONE', *, *, #8838, .F. ) ;
#32015=CIRCLE ( 'NONE', #26020, 0.7500000000000015543 ) ;
#32263=CARTESIAN_POINT ( 'NONE',  ( -2.600000000000000533, -11.64055411052240352, -1.199999999999999956 ) ) ;
#32564=AXIS2_PLACEMENT_3D ( 'NONE', #44954, #15815, #10808 ) ;
#32763=CARTESIAN_POINT ( 'NONE',  ( 0.000000000000000000, 0.000000000000000000, 0.000000000000000000 ) ) ;
#32866=DIRECTION ( 'NONE',  ( 0.000000000000000000, 0.000000000000000000, 1.000000000000000000 ) ) ;
#33039=ORIENTED_EDGE ( 'NONE', *, *, #15646, .T. ) ;
#33053=CARTESIAN_POINT ( 'NONE',  ( -6.890143360408123030, -11.60930335864404306, 0.000000000000000000 ) ) ;
#33091=DIRECTION ( 'NONE',  ( 0.000000000000000000, 0.000000000000000000, 1.000000000000000000 ) ) ;
#33179=ORIENTED_EDGE ( 'NONE', *, *, #5894, .T. ) ;
#33470=CARTESIAN_POINT ( 'NONE',  ( -0.2111111111111110827, -9.497654031326126400, -1.199999999999999956 ) ) ;
#33479=CARTESIAN_POINT ( 'NONE',  ( 3.514385190458181096, -13.03453477240704039, -1.199999999999999956 ) ) ;
#33586=DIRECTION ( 'NONE',  ( 1.000000000000000000, 0.000000000000000000, 0.000000000000000000 ) ) ;
#33676=AXIS2_PLACEMENT_3D ( 'NONE', #5625, #10994, #20384 ) ;
#33839=CARTESIAN_POINT ( 'NONE',  ( 0.000000000000000000, 0.6959691356230525150, 0.000000000000000000 ) ) ;
#33882=ORIENTED_EDGE ( 'NONE', *, *, #28804, .F. ) ;
#33899=EDGE_CURVE ( 'NONE', #13696, #11002, #26336, .T. ) ;
#33933=DIRECTION ( 'NONE',  ( 1.000000000000000000, 0.000000000000000000, 0.000000000000000000 ) ) ;
#33945=DIRECTION ( 'NONE',  ( 1.000000000000000000, 0.000000000000000000, 0.000000000000000000 ) ) ;
#33951=EDGE_CURVE ( 'NONE', #39805, #6056, #42855, .T. ) ;
#34016=CARTESIAN_POINT ( 'NONE',  ( -0.5999999999999992006, -11.64055411052240352, -1.199999999999999956 ) ) ;
#34033=CARTESIAN_POINT ( 'NONE',  ( 3.319141568766058814, -12.31039395171775830, -1.199999999999999956 ) ) ;
#34058=AXIS2_PLACEMENT_3D ( 'NONE', #45619, #26183, #26493 ) ;
#34093=AXIS2_PLACEMENT_3D ( 'NONE', #30822, #26130, #28288 ) ;
#34175=EDGE_CURVE ( 'NONE', #53602, #1542, #31823, .T. ) ;
#34181=VERTEX_POINT ( 'NONE', #37461 ) ;
#34191=ORIENTED_EDGE ( 'NONE', *, *, #61036, .T. ) ;
#34212=CIRCLE ( 'NONE', #44207, 2.698940690764988215 ) ;
#34276=DIRECTION ( 'NONE',  ( 0.000000000000000000, 0.000000000000000000, 1.000000000000000000 ) ) ;
#34472=CARTESIAN_POINT ( 'NONE',  ( 3.514385190458181096, -13.03453477240704039, 0.000000000000000000 ) ) ;
#34654=CIRCLE ( 'NONE', #33676, 11.40403086437694569 ) ;
#34671=EDGE_CURVE ( 'NONE', #2855, #56952, #28880, .T. ) ;
#34746=DIRECTION ( 'NONE',  ( 0.02222222222222222307, -0.9997530559290660479, 0.000000000000000000 ) ) ;
#34761=FILL_AREA_STYLE_COLOUR ( '', #45313 ) ;
#34778=CARTESIAN_POINT ( 'NONE',  ( -9.500000000000000000, 1.163414459189985485E-15, -1.199999999999999956 ) ) ;
#34820=EDGE_CURVE ( 'NONE', #23477, #13696, #34212, .T. ) ;
#34898=CARTESIAN_POINT ( 'NONE',  ( -1.600000000000000089, -11.64055411052240352, -1.199999999999999956 ) ) ;
#34925=DIRECTION ( 'NONE',  ( 1.000000000000000000, 0.000000000000000000, 0.000000000000000000 ) ) ;
#34940=ORIENTED_EDGE ( 'NONE', *, *, #59875, .F. ) ;
#35014=ORIENTED_EDGE ( 'NONE', *, *, #19966, .F. ) ;
#35186=DIRECTION ( 'NONE',  ( 1.000000000000000000, 0.000000000000000000, 0.000000000000000000 ) ) ;
#35202=CIRCLE ( 'NONE', #31153, 0.7500000000000015543 ) ;
#35261=DIRECTION ( 'NONE',  ( 1.000000000000000000, 0.000000000000000000, 0.000000000000000000 ) ) ;
#35334=ORIENTED_EDGE ( 'NONE', *, *, #55865, .T. ) ;
#35372=FILL_AREA_STYLE_COLOUR ( '', #42877 ) ;
#35463=FACE_OUTER_BOUND ( 'NONE', #45491, .T. ) ;
#35474=EDGE_LOOP ( 'NONE', ( #5245, #37262, #47812, #44298 ) ) ;
#35480=AXIS2_PLACEMENT_3D ( 'NONE', #48661, #23213, #9723 ) ;
#35711=EDGE_CURVE ( 'NONE', #19244, #53602, #14186, .T. ) ;
#35770=CARTESIAN_POINT ( 'NONE',  ( -6.890143360408123030, -11.60930335864404306, -1.199999999999999956 ) ) ;
#35787=ORIENTED_EDGE ( 'NONE', *, *, #44884, .F. ) ;
#35788=ORIENTED_EDGE ( 'NONE', *, *, #36445, .T. ) ;
#35928=ORIENTED_EDGE ( 'NONE', *, *, #25423, .F. ) ;
#36028=AXIS2_PLACEMENT_3D ( 'NONE', #56053, #23474, #47002 ) ;
#36044=CARTESIAN_POINT ( 'NONE',  ( -0.2111111111111110827, -9.497654031326126400, -1.199999999999999956 ) ) ;
#36102=EDGE_CURVE ( 'NONE', #20981, #23782, #34654, .T. ) ;
#36187=VECTOR ( 'NONE', #48004, 1000.000000000000114 ) ;
#36197=ORIENTED_EDGE ( 'NONE', *, *, #25423, .T. ) ;
#36226=ORIENTED_EDGE ( 'NONE', *, *, #29476, .F. ) ;
#36232=PLANE ( 'NONE',  #59182 ) ;
#36247=ORIENTED_EDGE ( 'NONE', *, *, #48085, .T. ) ;
#36249=DIRECTION ( 'NONE',  ( 0.000000000000000000, 0.000000000000000000, 1.000000000000000000 ) ) ;
#36253=VERTEX_POINT ( 'NONE', #40437 ) ;
#36275=CIRCLE ( 'NONE', #15297, 13.50000000000000178 ) ;
#36401=DIRECTION ( 'NONE',  ( 0.000000000000000000, 0.000000000000000000, 1.000000000000000000 ) ) ;
#36445=EDGE_CURVE ( 'NONE', #38091, #6280, #39827, .T. ) ;
#36496=VECTOR ( 'NONE', #7243, 1000.000000000000000 ) ;
#36680=AXIS2_PLACEMENT_3D ( 'NONE', #43519, #58802, #15925 ) ;
#36706=ORIENTED_EDGE ( 'NONE', *, *, #37427, .T. ) ;
#36784=UNCERTAINTY_MEASURE_WITH_UNIT (LENGTH_MEASURE( 1.000000000000000082E-05 ), #43873, 'distance_accuracy_value', 'NONE');
#36857=CARTESIAN_POINT ( 'NONE',  ( -3.319141568766058814, -12.31039395171775830, -1.199999999999999956 ) ) ;
#37094=AXIS2_PLACEMENT_3D ( 'NONE', #16053, #24509, #33933 ) ;
#37126=CARTESIAN_POINT ( 'NONE',  ( -6.890143360408123030, -11.60930335864404306, -1.199999999999999956 ) ) ;
#37193=DIRECTION ( 'NONE',  ( 1.000000000000000000, 0.000000000000000000, 0.000000000000000000 ) ) ;
#37262=ORIENTED_EDGE ( 'NONE', *, *, #38801, .F. ) ;
#37315=ORIENTED_EDGE ( 'NONE', *, *, #2639, .T. ) ;
#37427=EDGE_CURVE ( 'NONE', #13696, #6658, #45081, .T. ) ;
#37461=CARTESIAN_POINT ( 'NONE',  ( 4.214292481396495482, -11.25702090725073035, 0.000000000000000000 ) ) ;
#37470=DIRECTION ( 'NONE',  ( 0.000000000000000000, 0.000000000000000000, 1.000000000000000000 ) ) ;
#37622=CIRCLE ( 'NONE', #14593, 9.500000000000000000 ) ;
#37636=ORIENTED_EDGE ( 'NONE', *, *, #23113, .F. ) ;
#37814=EDGE_CURVE ( 'NONE', #24133, #11002, #5638, .T. ) ;
#37872=ADVANCED_FACE ( 'NONE', ( #39923 ), #14866, .F. ) ;
#37904=ORIENTED_EDGE ( 'NONE', *, *, #55865, .F. ) ;
#37930=DIRECTION ( 'NONE',  ( 0.000000000000000000, 0.000000000000000000, 1.000000000000000000 ) ) ;
#38085=VECTOR ( 'NONE', #46109, 1000.000000000000114 ) ;
#38091=VERTEX_POINT ( 'NONE', #10984 ) ;
#38112=FACE_OUTER_BOUND ( 'NONE', #20204, .T. ) ;
#38160=DIRECTION ( 'NONE',  ( 0.000000000000000000, 0.000000000000000000, 1.000000000000000000 ) ) ;
#38254=CARTESIAN_POINT ( 'NONE',  ( 0.000000000000000000, 0.000000000000000000, -1.199999999999999956 ) ) ;
#38314=CARTESIAN_POINT ( 'NONE',  ( 1.600000000000000089, -11.64055411052240352, 0.000000000000000000 ) ) ;
#38333=AXIS2_PLACEMENT_3D ( 'NONE', #3605, #55613, #13353 ) ;
#38377=DIRECTION ( 'NONE',  ( -0.000000000000000000, -0.000000000000000000, -1.000000000000000000 ) ) ;
#38506=DIRECTION ( 'NONE',  ( 1.000000000000000000, 0.000000000000000000, 0.000000000000000000 ) ) ;
#38526=CIRCLE ( 'NONE', #22548, 13.50000000000000178 ) ;
#38542=FACE_OUTER_BOUND ( 'NONE', #50269, .T. ) ;
#38588=DIRECTION ( 'NONE',  ( 1.000000000000000000, 0.000000000000000000, 0.000000000000000000 ) ) ;
#38682=VERTEX_POINT ( 'NONE', #61630 ) ;
#38713=EDGE_CURVE ( 'NONE', #38682, #55303, #20740, .T. ) ;
#38801=EDGE_CURVE ( 'NONE', #19244, #56336, #39419, .T. ) ;
#38813=EDGE_LOOP ( 'NONE', ( #30052, #2539, #11615, #44028 ) ) ;
#39014=AXIS2_PLACEMENT_3D ( 'NONE', #60025, #36249, #30589 ) ;
#39314=EDGE_LOOP ( 'NONE', ( #51469, #211, #28519, #37315 ) ) ;
#39318=AXIS2_PLACEMENT_3D ( 'NONE', #594, #49151, #57593 ) ;
#39419=LINE ( 'NONE', #33479, #2697 ) ;
#39456=( LENGTH_UNIT ( ) NAMED_UNIT ( * ) SI_UNIT ( .MILLI., .METRE. ) );
#39499=ORIENTED_EDGE ( 'NONE', *, *, #38713, .T. ) ;
#39572=ORIENTED_EDGE ( 'NONE', *, *, #17624, .F. ) ;
#39648=EDGE_LOOP ( 'NONE', ( #37636, #4468, #31300, #48841 ) ) ;
#39736=CARTESIAN_POINT ( 'NONE',  ( -9.500000000000000000, 1.163414459189985485E-15, 0.000000000000000000 ) ) ;
#39775=CARTESIAN_POINT ( 'NONE',  ( -0.2111111111111110827, -9.497654031326126400, 0.000000000000000000 ) ) ;
#39805=VERTEX_POINT ( 'NONE', #54094 ) ;
#39820=ORIENTED_EDGE ( 'NONE', *, *, #23271, .F. ) ;
#39827=CIRCLE ( 'NONE', #36680, 1.000000000000000666 ) ;
#39855=EDGE_CURVE ( 'NONE', #57538, #34181, #49414, .T. ) ;
#39923=FACE_OUTER_BOUND ( 'NONE', #23770, .T. ) ;
#40253=CARTESIAN_POINT ( 'NONE',  ( -1.600000000000000089, -11.64055411052240352, -1.199999999999999956 ) ) ;
#40437=CARTESIAN_POINT ( 'NONE',  ( 0.2999999999999897193, -13.49666625504239192, -1.199999999999999956 ) ) ;
#40439=CARTESIAN_POINT ( 'NONE',  ( 0.000000000000000000, 0.6959691356230525150, -1.199999999999999956 ) ) ;
#40671=CIRCLE ( 'NONE', #52606, 1.000000000000000888 ) ;
#40874=MECHANICAL_DESIGN_GEOMETRIC_PRESENTATION_REPRESENTATION('',(#46860),#29830);
#41055=ORIENTED_EDGE ( 'NONE', *, *, #23460, .T. ) ;
#41061=DIRECTION ( 'NONE',  ( 1.000000000000000000, 0.000000000000000000, 0.000000000000000000 ) ) ;
#41069=DIRECTION ( 'NONE',  ( 1.000000000000000000, 0.000000000000000000, 0.000000000000000000 ) ) ;
#41131=EDGE_CURVE ( 'NONE', #38091, #10566, #13907, .T. ) ;
#41137=CARTESIAN_POINT ( 'NONE',  ( 11.40403086437694569, 0.6959691356230525150, 0.000000000000000000 ) ) ;
#41242=ORIENTED_EDGE ( 'NONE', *, *, #54946, .T. ) ;
#41274=ADVANCED_FACE ( 'NONE', ( #23593 ), #5388, .T. ) ;
#41416=CARTESIAN_POINT ( 'NONE',  ( -4.062725214796418349, -12.40828859588279798, -1.199999999999999956 ) ) ;
#41508=VECTOR ( 'NONE', #31008, 1000.000000000000114 ) ;
#41585=CARTESIAN_POINT ( 'NONE',  ( -4.214292481396491930, -11.25702090725073035, 0.000000000000000000 ) ) ;
#41642=CARTESIAN_POINT ( 'NONE',  ( 4.062725214796417461, -12.40828859588279798, -1.199999999999999956 ) ) ;
#41804=FACE_OUTER_BOUND ( 'NONE', #52348, .T. ) ;
#42075=CARTESIAN_POINT ( 'NONE',  ( 6.890143360408123030, -11.60930335864404306, -1.199999999999999956 ) ) ;
#42078=PLANE ( 'NONE',  #59313 ) ;
#42162=CARTESIAN_POINT ( 'NONE',  ( -3.319141568766058814, -12.31039395171775830, -1.199999999999999956 ) ) ;
#42198=VERTEX_POINT ( 'NONE', #39736 ) ;
#42418=VECTOR ( 'NONE', #29678, 1000.000000000000000 ) ;
#42553=ORIENTED_EDGE ( 'NONE', *, *, #42871, .F. ) ;
#42675=DIRECTION ( 'NONE',  ( 0.000000000000000000, 0.000000000000000000, 1.000000000000000000 ) ) ;
#42855=LINE ( 'NONE', #29341, #28416 ) ;
#42871=EDGE_CURVE ( 'NONE', #57538, #28712, #52883, .T. ) ;
#42877=COLOUR_RGB ( '', 0.09019608, 0.27058824, 0.51372549) ;
#43047=CARTESIAN_POINT ( 'NONE',  ( -1.600000000000000089, -11.64055411052240352, -1.199999999999999956 ) ) ;
#43519=CARTESIAN_POINT ( 'NONE',  ( 1.600000000000000089, -11.64055411052240352, -1.199999999999999956 ) ) ;
#43567=EDGE_LOOP ( 'NONE', ( #6782, #47201, #48730, #9714 ) ) ;
#43618=CIRCLE ( 'NONE', #4573, 11.40403086437694569 ) ;
#43764=VECTOR ( 'NONE', #23901, 1000.000000000000000 ) ;
#43873=( LENGTH_UNIT ( ) NAMED_UNIT ( * ) SI_UNIT ( .MILLI., .METRE. ) );
#44028=ORIENTED_EDGE ( 'NONE', *, *, #33951, .T. ) ;
#44207=AXIS2_PLACEMENT_3D ( 'NONE', #35770, #12886, #2529 ) ;
#44298=ORIENTED_EDGE ( 'NONE', *, *, #34175, .T. ) ;
#44365=DIRECTION ( 'NONE',  ( -1.000000000000000000, 0.000000000000000000, 0.000000000000000000 ) ) ;
#44408=CARTESIAN_POINT ( 'NONE',  ( 0.000000000000000000, 0.6959691356230525150, -1.199999999999999956 ) ) ;
#44442=DIRECTION ( 'NONE',  ( 0.000000000000000000, 0.000000000000000000, 1.000000000000000000 ) ) ;
#44575=FACE_OUTER_BOUND ( 'NONE', #52861, .T. ) ;
#44795=( NAMED_UNIT ( * ) SI_UNIT ( $, .STERADIAN. ) SOLID_ANGLE_UNIT ( ) );
#44829=CIRCLE ( 'NONE', #52788, 0.7500000000000015543 ) ;
#44864=DIRECTION ( 'NONE',  ( 0.000000000000000000, 0.000000000000000000, 1.000000000000000000 ) ) ;
#44884=EDGE_CURVE ( 'NONE', #6088, #7385, #14951, .T. ) ;
#44911=ORIENTED_EDGE ( 'NONE', *, *, #41131, .T. ) ;
#44954=CARTESIAN_POINT ( 'NONE',  ( 0.000000000000000000, 0.000000000000000000, 0.000000000000000000 ) ) ;
#45081=LINE ( 'NONE', #2109, #52692 ) ;
#45168=CARTESIAN_POINT ( 'NONE',  ( -11.40403086437694569, 0.6959691356230539583, 0.000000000000000000 ) ) ;
#45174=FACE_OUTER_BOUND ( 'NONE', #23701, .T. ) ;
#45238=ADVANCED_FACE ( 'NONE', ( #15285 ), #14363, .T. ) ;
#45252=ORIENTED_EDGE ( 'NONE', *, *, #50444, .F. ) ;
#45268=DIRECTION ( 'NONE',  ( 0.000000000000000000, 0.000000000000000000, 1.000000000000000000 ) ) ;
#45313=COLOUR_RGB ( '', 0.09019608, 0.27058824, 0.51372549) ;
#45368=ADVANCED_FACE ( 'NONE', ( #12139 ), #21512, .T. ) ;
#45391=SURFACE_STYLE_USAGE ( .BOTH. , #59449 ) ;
#45408=VERTEX_POINT ( 'NONE', #31220 ) ;
#45464=CARTESIAN_POINT ( 'NONE',  ( 0.5999999999999994227, -11.64055411052240352, 0.000000000000000000 ) ) ;
#45491=EDGE_LOOP ( 'NONE', ( #50254, #51276, #51065, #57534, #52801, #11612, #33882, #7964, #34940, #42553, #60733, #60380, #2322, #35014, #60702, #35787 ) ) ;
#45500=ORIENTED_EDGE ( 'NONE', *, *, #34820, .T. ) ;
#45531=FACE_OUTER_BOUND ( 'NONE', #35474, .T. ) ;
#45559=VERTEX_POINT ( 'NONE', #34016 ) ;
#45562=ADVANCED_FACE ( 'NONE', ( #38112 ), #23979, .F. ) ;
#45619=CARTESIAN_POINT ( 'NONE',  ( 0.000000000000000000, 0.6959691356230525150, 0.000000000000000000 ) ) ;
#45784=CYLINDRICAL_SURFACE ( 'NONE', #20128, 9.500000000000000000 ) ;
#45867=AXIS2_PLACEMENT_3D ( 'NONE', #9212, #23623, #52732 ) ;
#45936=PRODUCT_CONTEXT ( 'NONE', #23534, 'mechanical' ) ;
#46109=DIRECTION ( 'NONE',  ( 0.1305261922200498526, 0.9914448613738106042, -0.000000000000000000 ) ) ;
#46158=EDGE_CURVE ( 'NONE', #45408, #6056, #32015, .T. ) ;
#46514=CIRCLE ( 'NONE', #27493, 1.000000000000000666 ) ;
#46588=ORIENTED_EDGE ( 'NONE', *, *, #33951, .F. ) ;
#46778=DIRECTION ( 'NONE',  ( 0.000000000000000000, 0.000000000000000000, 1.000000000000000000 ) ) ;
#46860=STYLED_ITEM ( 'NONE', ( #25954 ), #21278 ) ;
#47002=DIRECTION ( 'NONE',  ( 1.000000000000000000, 0.000000000000000000, 0.000000000000000000 ) ) ;
#47088=CARTESIAN_POINT ( 'NONE',  ( -9.500000000000000000, 1.163414459189985485E-15, -1.199999999999999956 ) ) ;
#47114=ORIENTED_EDGE ( 'NONE', *, *, #58527, .T. ) ;
#47152=DIRECTION ( 'NONE',  ( 1.000000000000000000, 0.000000000000000000, 0.000000000000000000 ) ) ;
#47201=ORIENTED_EDGE ( 'NONE', *, *, #23460, .F. ) ;
#47381=DIRECTION ( 'NONE',  ( 0.000000000000000000, 0.000000000000000000, 1.000000000000000000 ) ) ;
#47437=VECTOR ( 'NONE', #14040, 1000.000000000000000 ) ;
#47532=CARTESIAN_POINT ( 'NONE',  ( -4.214292481396491930, -11.25702090725073035, 0.000000000000000000 ) ) ;
#47546=VECTOR ( 'NONE', #11143, 1000.000000000000000 ) ;
#47704=ORIENTED_EDGE ( 'NONE', *, *, #58527, .F. ) ;
#47812=ORIENTED_EDGE ( 'NONE', *, *, #35711, .T. ) ;
#47909=ORIENTED_EDGE ( 'NONE', *, *, #53303, .F. ) ;
#48004=DIRECTION ( 'NONE',  ( 0.02222222222222222307, -0.9997530559290660479, 0.000000000000000000 ) ) ;
#48085=EDGE_CURVE ( 'NONE', #56336, #1542, #44829, .T. ) ;
#48415=DIRECTION ( 'NONE',  ( 0.000000000000000000, 0.000000000000000000, 1.000000000000000000 ) ) ;
#48661=CARTESIAN_POINT ( 'NONE',  ( 1.600000000000000089, -11.64055411052240352, 0.000000000000000000 ) ) ;
#48730=ORIENTED_EDGE ( 'NONE', *, *, #27876, .T. ) ;
#48808=EDGE_LOOP ( 'NONE', ( #47704, #46588, #9512, #18242 ) ) ;
#48841=ORIENTED_EDGE ( 'NONE', *, *, #26667, .T. ) ;
#48861=VECTOR ( 'NONE', #37930, 1000.000000000000000 ) ;
#48932=ORIENTED_EDGE ( 'NONE', *, *, #51962, .T. ) ;
#49151=DIRECTION ( 'NONE',  ( 0.000000000000000000, 0.000000000000000000, 1.000000000000000000 ) ) ;
#49176=AXIS2_PLACEMENT_3D ( 'NONE', #34033, #48415, #44365 ) ;
#49201=ORIENTED_EDGE ( 'NONE', *, *, #28804, .T. ) ;
#49268=EDGE_CURVE ( 'NONE', #45559, #31387, #4973, .T. ) ;
#49414=LINE ( 'NONE', #16851, #19679 ) ;
#49442=FILL_AREA_STYLE ('',( #35372 ) ) ;
#49525=CARTESIAN_POINT ( 'NONE',  ( 0.000000000000000000, 0.000000000000000000, 0.000000000000000000 ) ) ;
#49684=CARTESIAN_POINT ( 'NONE',  ( 4.214292481396495482, -11.25702090725073035, -1.199999999999999956 ) ) ;
#49822=VECTOR ( 'NONE', #31412, 1000.000000000000000 ) ;
#49969=LINE ( 'NONE', #1715, #5787 ) ;
#50037=VECTOR ( 'NONE', #36401, 1000.000000000000000 ) ;
#50100=VERTEX_POINT ( 'NONE', #28650 ) ;
#50254=ORIENTED_EDGE ( 'NONE', *, *, #8627, .F. ) ;
#50269=EDGE_LOOP ( 'NONE', ( #2258, #31927, #55779, #52339 ) ) ;
#50337=EDGE_LOOP ( 'NONE', ( #10421, #31079, #35928, #14300 ) ) ;
#50371=DIRECTION ( 'NONE',  ( 0.02222222222222222307, 0.9997530559290660479, -0.000000000000000000 ) ) ;
#50442=CIRCLE ( 'NONE', #23434, 9.500000000000000000 ) ;
#50444=EDGE_CURVE ( 'NONE', #6088, #42198, #55840, .T. ) ;
#50470=AXIS2_PLACEMENT_3D ( 'NONE', #12850, #50714, #41061 ) ;
#50654=CARTESIAN_POINT ( 'NONE',  ( 0.2999999999999897193, -13.49666625504239192, -1.199999999999999956 ) ) ;
#50714=DIRECTION ( 'NONE',  ( -0.000000000000000000, -0.000000000000000000, -1.000000000000000000 ) ) ;
#50783=PRODUCT_DEFINITION_SHAPE ( 'NONE', 'NONE',  #26005 ) ;
#50790=LINE ( 'NONE', #56104, #36496 ) ;
#50904=EDGE_CURVE ( 'NONE', #28712, #38682, #866, .T. ) ;
#51065=ORIENTED_EDGE ( 'NONE', *, *, #54654, .F. ) ;
#51276=ORIENTED_EDGE ( 'NONE', *, *, #8669, .F. ) ;
#51469=ORIENTED_EDGE ( 'NONE', *, *, #13855, .F. ) ;
#51485=DIRECTION ( 'NONE',  ( 0.000000000000000000, 0.000000000000000000, 1.000000000000000000 ) ) ;
#51664=CARTESIAN_POINT ( 'NONE',  ( 3.514385190458181096, -13.03453477240704039, -1.199999999999999956 ) ) ;
#51830=DIRECTION ( 'NONE',  ( 0.000000000000000000, 0.000000000000000000, 1.000000000000000000 ) ) ;
#51962=EDGE_CURVE ( 'NONE', #7385, #6350, #50442, .T. ) ;
#51986=AXIS2_PLACEMENT_3D ( 'NONE', #38254, #10345, #52933 ) ;
#52125=DIRECTION ( 'NONE',  ( -0.000000000000000000, -0.000000000000000000, -1.000000000000000000 ) ) ;
#52339=ORIENTED_EDGE ( 'NONE', *, *, #53303, .T. ) ;
#52348=EDGE_LOOP ( 'NONE', ( #19928, #44911, #57387, #13051 ) ) ;
#52394=ORIENTED_EDGE ( 'NONE', *, *, #50904, .T. ) ;
#52523=AXIS2_PLACEMENT_3D ( 'NONE', #30012, #29393, #15012 ) ;
#52606=AXIS2_PLACEMENT_3D ( 'NONE', #43047, #19536, #33945 ) ;
#52647=FACE_OUTER_BOUND ( 'NONE', #30428, .T. ) ;
#52682=DIRECTION ( 'NONE',  ( 1.000000000000000000, 0.000000000000000000, 0.000000000000000000 ) ) ;
#52692=VECTOR ( 'NONE', #10307, 1000.000000000000114 ) ;
#52732=DIRECTION ( 'NONE',  ( 1.000000000000000000, 0.000000000000000000, 0.000000000000000000 ) ) ;
#52780=DIRECTION ( 'NONE',  ( -0.000000000000000000, -0.000000000000000000, -1.000000000000000000 ) ) ;
#52788=AXIS2_PLACEMENT_3D ( 'NONE', #27326, #7268, #26396 ) ;
#52801=ORIENTED_EDGE ( 'NONE', *, *, #37427, .F. ) ;
#52807=AXIS2_PLACEMENT_3D ( 'NONE', #42075, #42675, #57342 ) ;
#52861=EDGE_LOOP ( 'NONE', ( #53073, #49201, #15313, #30929 ) ) ;
#52883=CIRCLE ( 'NONE', #29897, 2.698940690764985550 ) ;
#52933=DIRECTION ( 'NONE',  ( 1.000000000000000000, 0.000000000000000000, 0.000000000000000000 ) ) ;
#52978=CIRCLE ( 'NONE', #36028, 1.000000000000000888 ) ;
#53049=CARTESIAN_POINT ( 'NONE',  ( 4.062725214796417461, -12.40828859588279798, 0.000000000000000000 ) ) ;
#53073=ORIENTED_EDGE ( 'NONE', *, *, #49, .F. ) ;
#53169=CARTESIAN_POINT ( 'NONE',  ( 2.600000000000000533, -11.64055411052240352, -1.199999999999999956 ) ) ;
#53248=EDGE_LOOP ( 'NONE', ( #1150, #34191 ) ) ;
#53303=EDGE_CURVE ( 'NONE', #5698, #10566, #58460, .T. ) ;
#53306=ORIENTED_EDGE ( 'NONE', *, *, #33899, .F. ) ;
#53314=ORIENTED_EDGE ( 'NONE', *, *, #56980, .T. ) ;
#53475=ORIENTED_EDGE ( 'NONE', *, *, #30805, .T. ) ;
#53510=SURFACE_STYLE_FILL_AREA ( #49442 ) ;
#53600=ORIENTED_EDGE ( 'NONE', *, *, #39855, .F. ) ;
#53602=VERTEX_POINT ( 'NONE', #41642 ) ;
#53796=CARTESIAN_POINT ( 'NONE',  ( 0.2111111111111110827, -9.497654031326126400, -1.199999999999999956 ) ) ;
#53828=( NAMED_UNIT ( * ) PLANE_ANGLE_UNIT ( ) SI_UNIT ( $, .RADIAN. ) );
#53928=AXIS2_PLACEMENT_3D ( 'NONE', #25417, #7222, #30420 ) ;
#53939=ORIENTED_EDGE ( 'NONE', *, *, #141, .T. ) ;
#54094=CARTESIAN_POINT ( 'NONE',  ( -3.514385190458188646, -13.03453477240703862, -1.199999999999999956 ) ) ;
#54149=ORIENTED_EDGE ( 'NONE', *, *, #29476, .T. ) ;
#54154=ORIENTED_EDGE ( 'NONE', *, *, #17624, .T. ) ;
#54303=DIRECTION ( 'NONE',  ( 1.000000000000000000, 0.000000000000000000, 0.000000000000000000 ) ) ;
#54611=CYLINDRICAL_SURFACE ( 'NONE', #34093, 1.000000000000000666 ) ;
#54654=EDGE_CURVE ( 'NONE', #39805, #22852, #38526, .T. ) ;
#54756=PRODUCT ( 'circlip for shafts normal_din_Circlip DIN 471 - 20 x 1.2', 'circlip for shafts normal_din_Circlip DIN 471 - 20 x 1.2', '', ( #45936 ) ) ;
#54792=EDGE_LOOP ( 'NONE', ( #17079, #53314, #22967, #10794 ) ) ;
#54836=AXIS2_PLACEMENT_3D ( 'NONE', #28419, #18113, #4590 ) ;
#54897=AXIS2_PLACEMENT_3D ( 'NONE', #42162, #61215, #47152 ) ;
#54946=EDGE_CURVE ( 'NONE', #7385, #60067, #16447, .T. ) ;
#54949=DIRECTION ( 'NONE',  ( 0.000000000000000000, 0.000000000000000000, 1.000000000000000000 ) ) ;
#54976=SHAPE_DEFINITION_REPRESENTATION ( #50783, #13 ) ;
#55303=VERTEX_POINT ( 'NONE', #41137 ) ;
#55334=CARTESIAN_POINT ( 'NONE',  ( 0.000000000000000000, 0.000000000000000000, -1.199999999999999956 ) ) ;
#55467=CIRCLE ( 'NONE', #9459, 1.000000000000000666 ) ;
#55532=VERTEX_POINT ( 'NONE', #30387 ) ;
#55613=DIRECTION ( 'NONE',  ( -0.9997530559290660479, -0.02222222222222222307, 0.000000000000000000 ) ) ;
#55779=ORIENTED_EDGE ( 'NONE', *, *, #11348, .T. ) ;
#55840=LINE ( 'NONE', #47088, #13347 ) ;
#55865=EDGE_CURVE ( 'NONE', #8159, #42198, #22589, .T. ) ;
#55886=CYLINDRICAL_SURFACE ( 'NONE', #25706, 2.698940690764988215 ) ;
#55998=FACE_OUTER_BOUND ( 'NONE', #2225, .T. ) ;
#56053=CARTESIAN_POINT ( 'NONE',  ( -1.600000000000000089, -11.64055411052240352, -1.199999999999999956 ) ) ;
#56104=CARTESIAN_POINT ( 'NONE',  ( -0.2999999999999999889, -13.49666625504239015, -1.199999999999999956 ) ) ;
#56336=VERTEX_POINT ( 'NONE', #34472 ) ;
#56350=DIRECTION ( 'NONE',  ( 0.000000000000000000, 0.000000000000000000, 1.000000000000000000 ) ) ;
#56654=CARTESIAN_POINT ( 'NONE',  ( 6.890143360408123030, -11.60930335864404306, -1.199999999999999956 ) ) ;
#56751=CARTESIAN_POINT ( 'NONE',  ( -0.2111111111111110827, -9.497654031326126400, -1.199999999999999956 ) ) ;
#56785=CARTESIAN_POINT ( 'NONE',  ( 0.000000000000000000, 0.6959691356230525150, -1.199999999999999956 ) ) ;
#56919=CIRCLE ( 'NONE', #57892, 9.500000000000000000 ) ;
#56952=VERTEX_POINT ( 'NONE', #11394 ) ;
#56980=EDGE_CURVE ( 'NONE', #20981, #55303, #3206, .T. ) ;
#57154=DIRECTION ( 'NONE',  ( 1.000000000000000000, 0.000000000000000000, 0.000000000000000000 ) ) ;
#57342=DIRECTION ( 'NONE',  ( 1.000000000000000000, 0.000000000000000000, 0.000000000000000000 ) ) ;
#57365=DIRECTION ( 'NONE',  ( 0.000000000000000000, 0.000000000000000000, 1.000000000000000000 ) ) ;
#57387=ORIENTED_EDGE ( 'NONE', *, *, #58060, .T. ) ;
#57390=CARTESIAN_POINT ( 'NONE',  ( -0.2111111111111110827, -9.497654031326126400, 0.000000000000000000 ) ) ;
#57425=DIRECTION ( 'NONE',  ( 1.000000000000000000, 0.000000000000000000, 0.000000000000000000 ) ) ;
#57534=ORIENTED_EDGE ( 'NONE', *, *, #15386, .F. ) ;
#57538=VERTEX_POINT ( 'NONE', #49684 ) ;
#57570=DIRECTION ( 'NONE',  ( 1.000000000000000000, 0.000000000000000000, 0.000000000000000000 ) ) ;
#57593=DIRECTION ( 'NONE',  ( 1.000000000000000000, 0.000000000000000000, 0.000000000000000000 ) ) ;
#57879=DIRECTION ( 'NONE',  ( -0.000000000000000000, -0.000000000000000000, -1.000000000000000000 ) ) ;
#57892=AXIS2_PLACEMENT_3D ( 'NONE', #19261, #38377, #57425 ) ;
#58060=EDGE_CURVE ( 'NONE', #10566, #5698, #46514, .T. ) ;
#58162=DIRECTION ( 'NONE',  ( 0.02222222222222222307, 0.9997530559290660479, 0.000000000000000000 ) ) ;
#58453=CIRCLE ( 'NONE', #31467, 1.000000000000000888 ) ;
#58460=CIRCLE ( 'NONE', #35480, 1.000000000000000666 ) ;
#58512=( LENGTH_UNIT ( ) NAMED_UNIT ( * ) SI_UNIT ( .MILLI., .METRE. ) );
#58514=CARTESIAN_POINT ( 'NONE',  ( 0.2111111111111110827, -9.497654031326126400, -1.199999999999999956 ) ) ;
#58527=EDGE_CURVE ( 'NONE', #6056, #26491, #28557, .T. ) ;
#58597=VECTOR ( 'NONE', #50371, 1000.000000000000114 ) ;
#58802=DIRECTION ( 'NONE',  ( 0.000000000000000000, 0.000000000000000000, 1.000000000000000000 ) ) ;
#59170=CARTESIAN_POINT ( 'NONE',  ( -3.514385190458188646, -13.03453477240703862, 0.000000000000000000 ) ) ;
#59182=AXIS2_PLACEMENT_3D ( 'NONE', #32763, #60936, #18359 ) ;
#59307=DIRECTION ( 'NONE',  ( 0.000000000000000000, 0.000000000000000000, 1.000000000000000000 ) ) ;
#59313=AXIS2_PLACEMENT_3D ( 'NONE', #61130, #61429, #27636 ) ;
#59449=SURFACE_SIDE_STYLE ('',( #53510 ) ) ;
#59553=CARTESIAN_POINT ( 'NONE',  ( 4.214292481396495482, -11.25702090725073035, 0.000000000000000000 ) ) ;
#59556=CARTESIAN_POINT ( 'NONE',  ( 2.600000000000000533, -11.64055411052240352, 0.000000000000000000 ) ) ;
#59578=CARTESIAN_POINT ( 'NONE',  ( -1.600000000000000089, -11.64055411052240352, 0.000000000000000000 ) ) ;
#59596=CYLINDRICAL_SURFACE ( 'NONE', #6175, 0.7500000000000015543 ) ;
#59754=EDGE_CURVE ( 'NONE', #42198, #60067, #37622, .T. ) ;
#59875=EDGE_CURVE ( 'NONE', #28712, #20981, #43618, .T. ) ;
#60025=CARTESIAN_POINT ( 'NONE',  ( 0.000000000000000000, 0.000000000000000000, -1.199999999999999956 ) ) ;
#60067=VERTEX_POINT ( 'NONE', #21745 ) ;
#60304=FACE_OUTER_BOUND ( 'NONE', #8820, .T. ) ;
#60380=ORIENTED_EDGE ( 'NONE', *, *, #35711, .F. ) ;
#60420=VECTOR ( 'NONE', #51830, 1000.000000000000000 ) ;
#60460=DIRECTION ( 'NONE',  ( -0.000000000000000000, -0.000000000000000000, -1.000000000000000000 ) ) ;
#60470=CIRCLE ( 'NONE', #50470, 9.500000000000000000 ) ;
#60611=ORIENTED_EDGE ( 'NONE', *, *, #37814, .F. ) ;
#60660=CARTESIAN_POINT ( 'NONE',  ( -5.571549742892843327, -9.254395351074540699, -1.199999999999999956 ) ) ;
#60702=ORIENTED_EDGE ( 'NONE', *, *, #51962, .F. ) ;
#60733=ORIENTED_EDGE ( 'NONE', *, *, #26361, .F. ) ;
#60936=DIRECTION ( 'NONE',  ( 0.000000000000000000, 0.000000000000000000, 1.000000000000000000 ) ) ;
#61006=PLANE ( 'NONE',  #54836 ) ;
#61019=CLOSED_SHELL ( 'NONE', ( #37872, #780, #25310, #41274, #22863, #45562, #2842, #45238, #45368, #29482, #7071, #61856, #1059, #26957, #31880, #16439, #9764, #31725, #4847, #15381, #31242, #12485 ) ) ;
#61036=EDGE_CURVE ( 'NONE', #55532, #45559, #40671, .T. ) ;
#61130=CARTESIAN_POINT ( 'NONE',  ( 4.214292481396495482, -11.25702090725073035, -1.199999999999999956 ) ) ;
#61161=UNCERTAINTY_MEASURE_WITH_UNIT (LENGTH_MEASURE( 1.000000000000000082E-05 ), #39456, 'distance_accuracy_value', 'NONE');
#61215=DIRECTION ( 'NONE',  ( 0.000000000000000000, 0.000000000000000000, 1.000000000000000000 ) ) ;
#61275=STYLED_ITEM ( 'NONE', ( #5895 ), #31244 ) ;
#61370=CARTESIAN_POINT ( 'NONE',  ( -0.5999999999999992006, -11.64055411052240352, -1.199999999999999956 ) ) ;
#61387=DIRECTION ( 'NONE',  ( 0.000000000000000000, 0.000000000000000000, 1.000000000000000000 ) ) ;
#61429=DIRECTION ( 'NONE',  ( 0.9914448613738107152, -0.1305261922200498526, 0.000000000000000000 ) ) ;
#61433=CARTESIAN_POINT ( 'NONE',  ( 0.000000000000000000, 0.000000000000000000, -1.199999999999999956 ) ) ;
#61630=CARTESIAN_POINT ( 'NONE',  ( 5.571549742892842438, -9.254395351074542475, 0.000000000000000000 ) ) ;
#61632=ORIENTED_EDGE ( 'NONE', *, *, #46158, .T. ) ;
#61658=LINE ( 'NONE', #32263, #12950 ) ;
#61769=CARTESIAN_POINT ( 'NONE',  ( -0.2999999999999999889, -13.49666625504239015, -1.199999999999999956 ) ) ;
#61856=ADVANCED_FACE ( 'NONE', ( #23015 ), #55886, .F. ) ;
#61910=AXIS2_PLACEMENT_3D ( 'NONE', #40439, #6549, #41069 ) ;
#61951=AXIS2_PLACEMENT_3D ( 'NONE', #15700, #19784, #38588 ) ;
ENDSEC;
END-ISO-10303-21;
